ISO-10303-21;
HEADER;
/* Generated by software containing ST-Developer
 * from STEP Tools, Inc. (www.steptools.com) 
 */

FILE_DESCRIPTION(
/* description */ ('Bin tilter linkage'),
/* implementation_level */ '2;1');

FILE_NAME(
/* name */ 'M4 short cap screw (21).step',
/* time_stamp */ '2026-10-28T03:26:24-07:00',
/* author */ (''),
/* organization */ (''),
/* preprocessor_version */ 'ST-DEVELOPER v20.2',
/* originating_system */ 'Autodesk Translation Framework v15.17.0.0',
/* authorisation */ '');

FILE_SCHEMA (('AUTOMOTIVE_DESIGN { 1 0 10303 214 3 1 1 }'));
ENDSEC;

DATA;
#10=MECHANICAL_DESIGN_GEOMETRIC_PRESENTATION_REPRESENTATION('',(#921),#23728);
#709=SHAPE_REPRESENTATION_RELATIONSHIP('SRR','None',#24175,#815);
#815=ADVANCED_BREP_SHAPE_REPRESENTATION('',(#1034),#23675);
#921=STYLED_ITEM('',(#24772),#1034);
#1034=MANIFOLD_SOLID_BREP('Body1',#12452);
#1355=FACE_BOUND('',#3370,.T.);
#1700=PLANE('',#14622);
#1701=PLANE('',#14627);
#1702=PLANE('',#14630);
#2324=FACE_OUTER_BOUND('',#3369,.T.);
#2325=FACE_OUTER_BOUND('',#3371,.T.);
#2326=FACE_OUTER_BOUND('',#3372,.T.);
#2327=FACE_OUTER_BOUND('',#3373,.T.);
#2328=FACE_OUTER_BOUND('',#3374,.T.);
#3369=EDGE_LOOP('',(#10009));
#3370=EDGE_LOOP('',(#10010));
#3371=EDGE_LOOP('',(#10011,#10012,#10013,#10014));
#3372=EDGE_LOOP('',(#10015));
#3373=EDGE_LOOP('',(#10016,#10017,#10018,#10019));
#3374=EDGE_LOOP('',(#10020));
#4219=LINE('',#21613,#4894);
#4220=LINE('',#21617,#4895);
#4894=VECTOR('',#17746,0.350000000000001);
#4895=VECTOR('',#17751,0.199999999999999);
#5647=CIRCLE('',#14623,0.350000000000001);
#5648=CIRCLE('',#14624,0.199999999999999);
#5649=CIRCLE('',#14626,0.350000000000001);
#5650=CIRCLE('',#14629,0.199999999999999);
#6501=VERTEX_POINT('',#21606);
#6502=VERTEX_POINT('',#21608);
#6503=VERTEX_POINT('',#21611);
#6504=VERTEX_POINT('',#21616);
#7744=EDGE_CURVE('',#6501,#6501,#5647,.T.);
#7745=EDGE_CURVE('',#6502,#6502,#5648,.T.);
#7746=EDGE_CURVE('',#6503,#6503,#5649,.T.);
#7747=EDGE_CURVE('',#6503,#6501,#4219,.T.);
#7748=EDGE_CURVE('',#6502,#6504,#4220,.T.);
#7749=EDGE_CURVE('',#6504,#6504,#5650,.T.);
#10009=ORIENTED_EDGE('',*,*,#7744,.F.);
#10010=ORIENTED_EDGE('',*,*,#7745,.T.);
#10011=ORIENTED_EDGE('',*,*,#7746,.F.);
#10012=ORIENTED_EDGE('',*,*,#7747,.T.);
#10013=ORIENTED_EDGE('',*,*,#7744,.T.);
#10014=ORIENTED_EDGE('',*,*,#7747,.F.);
#10015=ORIENTED_EDGE('',*,*,#7746,.T.);
#10016=ORIENTED_EDGE('',*,*,#7745,.F.);
#10017=ORIENTED_EDGE('',*,*,#7748,.T.);
#10018=ORIENTED_EDGE('',*,*,#7749,.T.);
#10019=ORIENTED_EDGE('',*,*,#7748,.F.);
#10020=ORIENTED_EDGE('',*,*,#7749,.F.);
#11489=CYLINDRICAL_SURFACE('',#14625,0.350000000000001);
#11490=CYLINDRICAL_SURFACE('',#14628,0.199999999999999);
#12049=ADVANCED_FACE('',(#2324,#1355),#1700,.F.);
#12050=ADVANCED_FACE('',(#2325),#11489,.T.);
#12051=ADVANCED_FACE('',(#2326),#1701,.T.);
#12052=ADVANCED_FACE('',(#2327),#11490,.T.);
#12053=ADVANCED_FACE('',(#2328),#1702,.F.);
#12452=CLOSED_SHELL('',(#12049,#12050,#12051,#12052,#12053));
#14621=AXIS2_PLACEMENT_3D('',#21604,#17734,#17735);
#14622=AXIS2_PLACEMENT_3D('',#21605,#17736,#17737);
#14623=AXIS2_PLACEMENT_3D('',#21607,#17738,#17739);
#14624=AXIS2_PLACEMENT_3D('',#21609,#17740,#17741);
#14625=AXIS2_PLACEMENT_3D('',#21610,#17742,#17743);
#14626=AXIS2_PLACEMENT_3D('',#21612,#17744,#17745);
#14627=AXIS2_PLACEMENT_3D('',#21614,#17747,#17748);
#14628=AXIS2_PLACEMENT_3D('',#21615,#17749,#17750);
#14629=AXIS2_PLACEMENT_3D('',#21618,#17752,#17753);
#14630=AXIS2_PLACEMENT_3D('',#21619,#17754,#17755);
#17734=DIRECTION('axis',(0.,0.,1.));
#17735=DIRECTION('refdir',(1.,0.,0.));
#17736=DIRECTION('center_axis',(0.,1.,0.));
#17737=DIRECTION('ref_axis',(1.,0.,0.));
#17738=DIRECTION('center_axis',(0.,1.,0.));
#17739=DIRECTION('ref_axis',(1.,0.,0.));
#17740=DIRECTION('center_axis',(0.,1.,0.));
#17741=DIRECTION('ref_axis',(1.,0.,0.));
#17742=DIRECTION('center_axis',(0.,1.,0.));
#17743=DIRECTION('ref_axis',(1.,0.,0.));
#17744=DIRECTION('center_axis',(0.,1.,0.));
#17745=DIRECTION('ref_axis',(1.,0.,0.));
#17746=DIRECTION('',(0.,-1.,0.));
#17747=DIRECTION('center_axis',(0.,1.,0.));
#17748=DIRECTION('ref_axis',(1.,0.,0.));
#17749=DIRECTION('center_axis',(0.,1.,0.));
#17750=DIRECTION('ref_axis',(1.,0.,0.));
#17751=DIRECTION('',(0.,-1.,0.));
#17752=DIRECTION('center_axis',(0.,1.,0.));
#17753=DIRECTION('ref_axis',(1.,0.,0.));
#17754=DIRECTION('center_axis',(0.,1.,0.));
#17755=DIRECTION('ref_axis',(1.,0.,0.));
#21604=CARTESIAN_POINT('',(0.,0.,0.));
#21605=CARTESIAN_POINT('Origin',(16.6918524548049,0.8,16.3081475451951));
#21606=CARTESIAN_POINT('',(16.3418524548049,0.8,16.3081475451951));
#21607=CARTESIAN_POINT('Origin',(16.6918524548049,0.8,16.3081475451951));
#21608=CARTESIAN_POINT('',(16.4918524548049,0.8,16.3081475451951));
#21609=CARTESIAN_POINT('Origin',(16.6918524548049,0.8,16.3081475451951));
#21610=CARTESIAN_POINT('Origin',(16.6918524548049,0.8,16.3081475451951));
#21611=CARTESIAN_POINT('',(16.3418524548049,1.2,16.3081475451951));
#21612=CARTESIAN_POINT('Origin',(16.6918524548049,1.2,16.3081475451951));
#21613=CARTESIAN_POINT('',(16.3418524548049,0.8,16.3081475451951));
#21614=CARTESIAN_POINT('Origin',(16.6918524548049,1.2,16.3081475451951));
#21615=CARTESIAN_POINT('Origin',(16.6918524548049,0.1,16.3081475451951));
#21616=CARTESIAN_POINT('',(16.4918524548049,0.1,16.3081475451951));
#21617=CARTESIAN_POINT('',(16.4918524548049,0.1,16.3081475451951));
#21618=CARTESIAN_POINT('Origin',(16.6918524548049,0.1,16.3081475451951));
#21619=CARTESIAN_POINT('Origin',(16.6918524548049,0.1,16.3081475451951));
#23558=UNCERTAINTY_MEASURE_WITH_UNIT(LENGTH_MEASURE(0.001),#23729,
'DISTANCE_ACCURACY_VALUE',
'Maximum model space distance between geometric entities at asserted c
onnectivities');
#23611=UNCERTAINTY_MEASURE_WITH_UNIT(LENGTH_MEASURE(0.001),#23729,
'DISTANCE_ACCURACY_VALUE',
'Maximum model space distance between geometric entities at asserted c
onnectivities');
#23675=(
GEOMETRIC_REPRESENTATION_CONTEXT(3)
GLOBAL_UNCERTAINTY_ASSIGNED_CONTEXT((#23558))
GLOBAL_UNIT_ASSIGNED_CONTEXT((#23729,#23731,#23732))
REPRESENTATION_CONTEXT('','3D')
);
#23728=(
GEOMETRIC_REPRESENTATION_CONTEXT(3)
GLOBAL_UNCERTAINTY_ASSIGNED_CONTEXT((#23611))
GLOBAL_UNIT_ASSIGNED_CONTEXT((#23729,#23731,#23732))
REPRESENTATION_CONTEXT('','3D')
);
#23729=(
LENGTH_UNIT()
NAMED_UNIT(*)
SI_UNIT(.CENTI.,.METRE.)
);
#23731=(
NAMED_UNIT(*)
PLANE_ANGLE_UNIT()
SI_UNIT($,.RADIAN.)
);
#23732=(
NAMED_UNIT(*)
SI_UNIT($,.STERADIAN.)
SOLID_ANGLE_UNIT()
);
#23796=SHAPE_DEFINITION_REPRESENTATION(#23912,#24175);
#23912=PRODUCT_DEFINITION_SHAPE('',$,#24292);
#24175=SHAPE_REPRESENTATION('',(#14621),#23675);
#24228=PRODUCT_DEFINITION_CONTEXT('part definition',#24578,'design');
#24292=PRODUCT_DEFINITION('M4 short cap screw (21)',
'M4 short cap screw (21)',#24408,#24228);
#24408=PRODUCT_DEFINITION_FORMATION('',$,#24643);
#24578=APPLICATION_CONTEXT(
'Core Data for Automotive Mechanical Design Process');
#24579=PRODUCT_CONTEXT('part definition',#24578,'mechanical');
#24643=PRODUCT('M4 short cap screw (21)','M4 short cap screw (21)',
'M4 short cap screw (21)',(#24579));
#24766=COLOUR_RGB('Black',0.12,0.14,0.17);
#24767=FILL_AREA_STYLE_COLOUR('',#24766);
#24768=FILL_AREA_STYLE('',(#24767));
#24769=SURFACE_STYLE_FILL_AREA(#24768);
#24770=SURFACE_SIDE_STYLE('',(#24769));
#24771=SURFACE_STYLE_USAGE(.BOTH.,#24770);
#24772=PRESENTATION_STYLE_ASSIGNMENT((#24771));
ENDSEC;
END-ISO-10303-21;
